ISO-10303-21;
HEADER;
FILE_DESCRIPTION (('STEP AP214'),
    '1' );
FILE_NAME ('socket head cap screw_iso_ISO 4762 M5 x 12 - 12N.step',
    '2026-10-08T13:56:24',
    ( '' ),
    ( '' ),
    'SwSTEP 2.0',
    'SolidWorks 2026',
    '' );
FILE_SCHEMA (( 'AUTOMOTIVE_DESIGN' ));
ENDSEC;

DATA;
#9=DIRECTION ( 'NONE',  ( -1.000000000000000000, -0.000000000000000000, -0.000000000000000000 ) ) ;
#22=EDGE_CURVE ( 'NONE', #14589, #7997, #9723, .T. ) ;
#88=CARTESIAN_POINT ( 'NONE',  ( 16.55500000000001393, 0.000000000000000000, 2.500000000000000444 ) ) ;
#107=CARTESIAN_POINT ( 'NONE',  ( 5.000000000000004441, 5.204748896376250699E-16, -4.250000000000000000 ) ) ;
#109=ORIENTED_EDGE ( 'NONE', *, *, #12160, .T. ) ;
#131=AXIS2_PLACEMENT_3D ( 'NONE', #700, #8225, #6765 ) ;
#148=CARTESIAN_POINT ( 'NONE',  ( -31.74999999999995737, 0.000000000000000000, 4.250000000000000000 ) ) ;
#189=CLOSED_SHELL ( 'NONE', ( #8416, #4530, #5345, #11458, #1142, #6838, #2428, #15032, #9127, #8023, #1756, #11349, #15010, #2861, #6382, #12271, #10045, #7422, #518, #1324, #8465, #1380, #7833, #9352, #14029, #11070, #15391 ) ) ;
#194=CIRCLE ( 'NONE', #13575, 2.500000000000000444 ) ;
#220=DIRECTION ( 'NONE',  ( -1.000000000000000000, -0.000000000000000000, -0.000000000000000000 ) ) ;
#221=DIRECTION ( 'NONE',  ( -1.000000000000000000, -0.000000000000000000, -0.000000000000000000 ) ) ;
#232=CARTESIAN_POINT ( 'NONE',  ( 0.000000000000000000, 0.000000000000000000, 0.000000000000000000 ) ) ;
#332=CARTESIAN_POINT ( 'NONE',  ( 0.000000000000000000, -1.178949249685213863, 2.042000000000002924 ) ) ;
#412=DIRECTION ( 'NONE',  ( 0.000000000000000000, 0.000000000000000000, 1.000000000000000000 ) ) ;
#419=ORIENTED_EDGE ( 'NONE', *, *, #12438, .F. ) ;
#433=ORIENTED_EDGE ( 'NONE', *, *, #4049, .T. ) ;
#501=PRODUCT_DEFINITION ( 'UNKNOWN', '', #14374, #14001 ) ;
#511=AXIS2_PLACEMENT_3D ( 'NONE', #3359, #10867, #8309 ) ;
#518=ADVANCED_FACE ( 'NONE', ( #10565 ), #8302, .F. ) ;
#587=LINE ( 'NONE', #1466, #12695 ) ;
#616=CARTESIAN_POINT ( 'NONE',  ( 2.500000000000000000, 0.000000000000000000, 0.000000000000000000 ) ) ;
#656=EDGE_CURVE ( 'NONE', #7770, #11426, #2343, .T. ) ;
#697=DIRECTION ( 'NONE',  ( 0.000000000000000000, -1.287488025362403787E-15, -1.000000000000000000 ) ) ;
#700=CARTESIAN_POINT ( 'NONE',  ( 2.500000000000000000, 0.000000000000000000, 0.000000000000000000 ) ) ;
#740=LINE ( 'NONE', #12919, #14172 ) ;
#771=DIRECTION ( 'NONE',  ( 0.000000000000000000, 0.000000000000000000, 1.000000000000000000 ) ) ;
#780=EDGE_CURVE ( 'NONE', #7205, #11041, #8594, .T. ) ;
#819=EDGE_CURVE ( 'NONE', #11041, #1955, #9872, .T. ) ;
#834=DIRECTION ( 'NONE',  ( 0.000000000000000000, -1.000000000000000000, 1.287488025362403787E-15 ) ) ;
#888=EDGE_CURVE ( 'NONE', #7896, #6707, #587, .T. ) ;
#889=PLANE ( 'NONE',  #14594 ) ;
#894=COLOUR_RGB ( '', 0.40784314, 0.44705882, 0.49803922) ;
#904=CARTESIAN_POINT ( 'NONE',  ( 0.000000000000000000, -1.178949249685213863, 2.042000000000002924 ) ) ;
#922=ORIENTED_EDGE ( 'NONE', *, *, #9390, .F. ) ;
#924=PLANE ( 'NONE',  #8231 ) ;
#948=ORIENTED_EDGE ( 'NONE', *, *, #3086, .T. ) ;
#997=DIRECTION ( 'NONE',  ( 0.000000000000000000, -1.224646799147353454E-16, 1.000000000000000000 ) ) ;
#1033=DIRECTION ( 'NONE',  ( 0.000000000000000000, 0.000000000000000000, 1.000000000000000000 ) ) ;
#1059=CARTESIAN_POINT ( 'NONE',  ( 2.500000000000000000, 2.357898499370433054, -1.951563910473907981E-15 ) ) ;
#1092=VECTOR ( 'NONE', #10245, 1000.000000000000000 ) ;
#1098=DIRECTION ( 'NONE',  ( 0.000000000000000000, 0.000000000000000000, -1.000000000000000000 ) ) ;
#1109=CIRCLE ( 'NONE', #8357, 4.250000000000000000 ) ;
#1135=ORIENTED_EDGE ( 'NONE', *, *, #12438, .T. ) ;
#1137=( GEOMETRIC_REPRESENTATION_CONTEXT ( 3 ) GLOBAL_UNCERTAINTY_ASSIGNED_CONTEXT ( ( #1398 ) ) GLOBAL_UNIT_ASSIGNED_CONTEXT ( ( #4736, #5875, #7019 ) ) REPRESENTATION_CONTEXT ( 'NONE', 'WORKASPACE' ) );
#1142=ADVANCED_FACE ( 'NONE', ( #12113 ), #7524, .T. ) ;
#1146=CARTESIAN_POINT ( 'NONE',  ( 2.500000000000000000, 1.178949249685213863, -2.042000000000001148 ) ) ;
#1216=DIRECTION ( 'NONE',  ( 0.000000000000000000, -0.5000000000000012212, -0.8660254037844380415 ) ) ;
#1218=CARTESIAN_POINT ( 'NONE',  ( 5.000000000000000888, 0.000000000000000000, 0.000000000000000000 ) ) ;
#1300=DIRECTION ( 'NONE',  ( 0.000000000000000000, 0.000000000000000000, -1.000000000000000000 ) ) ;
#1310=ORIENTED_EDGE ( 'NONE', *, *, #5864, .F. ) ;
#1324=ADVANCED_FACE ( 'NONE', ( #11618 ), #4190, .F. ) ;
#1364=CARTESIAN_POINT ( 'NONE',  ( 2.500000000000000000, 0.000000000000000000, 0.000000000000000000 ) ) ;
#1380=ADVANCED_FACE ( 'NONE', ( #7774 ), #6544, .F. ) ;
#1398=UNCERTAINTY_MEASURE_WITH_UNIT (LENGTH_MEASURE( 1.000000000000000082E-05 ), #4736, 'distance_accuracy_value', 'NONE');
#1420=STYLED_ITEM ( 'NONE', ( #5368 ), #14097 ) ;
#1466=CARTESIAN_POINT ( 'NONE',  ( 2.500000000000000000, -2.357898499370432610, 3.252606517456513302E-15 ) ) ;
#1492=DIRECTION ( 'NONE',  ( -0.5000000000000051070, 1.060575238724903217E-16, -0.8660254037844355990 ) ) ;
#1567=CARTESIAN_POINT ( 'NONE',  ( 2.500000000000000000, 2.500728763858895382E-16, -2.041999999999999815 ) ) ;
#1584=LINE ( 'NONE', #12719, #11976 ) ;
#1605=CARTESIAN_POINT ( 'NONE',  ( 2.500000000000000000, 2.357898499370433054, -1.951563910473907981E-15 ) ) ;
#1608=CARTESIAN_POINT ( 'NONE',  ( 2.500000000000000000, 1.178949249685218525, 2.041999999999999371 ) ) ;
#1617=ORIENTED_EDGE ( 'NONE', *, *, #5827, .F. ) ;
#1651=VERTEX_POINT ( 'NONE', #5883 ) ;
#1660=FACE_OUTER_BOUND ( 'NONE', #1712, .T. ) ;
#1698=VERTEX_POINT ( 'NONE', #7421 ) ;
#1712=EDGE_LOOP ( 'NONE', ( #11511, #6827, #8550, #14364 ) ) ;
#1756=ADVANCED_FACE ( 'NONE', ( #11201, #8795 ), #13699, .T. ) ;
#1795=ORIENTED_EDGE ( 'NONE', *, *, #819, .T. ) ;
#1796=EDGE_CURVE ( 'NONE', #15821, #6007, #5306, .T. ) ;
#1799=CARTESIAN_POINT ( 'NONE',  ( 2.500000000000000000, 2.357898499370433054, -1.951563910473907981E-15 ) ) ;
#1834=CARTESIAN_POINT ( 'NONE',  ( 0.000000000000000000, 1.178949249685213863, -2.042000000000001148 ) ) ;
#1892=ORIENTED_EDGE ( 'NONE', *, *, #8122, .T. ) ;
#1911=ORIENTED_EDGE ( 'NONE', *, *, #7555, .T. ) ;
#1929=VERTEX_POINT ( 'NONE', #1983 ) ;
#1955=VERTEX_POINT ( 'NONE', #7246 ) ;
#1966=CARTESIAN_POINT ( 'NONE',  ( 16.55500000000001393, 0.000000000000000000, 0.000000000000000000 ) ) ;
#1983=CARTESIAN_POINT ( 'NONE',  ( 5.000000000000004441, 0.000000000000000000, 4.250000000000000000 ) ) ;
#1996=SURFACE_STYLE_USAGE ( .BOTH. , #11997 ) ;
#2014=FACE_OUTER_BOUND ( 'NONE', #2418, .T. ) ;
#2017=CARTESIAN_POINT ( 'NONE',  ( 2.500000000000000000, -1.178949249685213863, 2.042000000000002924 ) ) ;
#2049=DIRECTION ( 'NONE',  ( -1.000000000000000000, -0.000000000000000000, -0.000000000000000000 ) ) ;
#2113=DIRECTION ( 'NONE',  ( -1.000000000000000000, -0.000000000000000000, -0.000000000000000000 ) ) ;
#2180=DIRECTION ( 'NONE',  ( 0.000000000000000000, 0.000000000000000000, 1.000000000000000000 ) ) ;
#2182=CIRCLE ( 'NONE', #15101, 2.700000000000000622 ) ;
#2207=ORIENTED_EDGE ( 'NONE', *, *, #9075, .T. ) ;
#2230=AXIS2_PLACEMENT_3D ( 'NONE', #8871, #9906, #8713 ) ;
#2244=CARTESIAN_POINT ( 'NONE',  ( 2.500000000000000000, 0.000000000000000000, 0.000000000000000000 ) ) ;
#2267=EDGE_LOOP ( 'NONE', ( #922, #2540, #10016 ) ) ;
#2288=CONICAL_SURFACE ( 'NONE', #11326, 2.055000000000000160, 0.7853981633974633780 ) ;
#2299=CARTESIAN_POINT ( 'NONE',  ( 5.200000000000002842, 0.000000000000000000, 2.500000000000000444 ) ) ;
#2343=LINE ( 'NONE', #3799, #14793 ) ;
#2358=CARTESIAN_POINT ( 'NONE',  ( 2.500000000000000000, 1.178949249685213863, -2.042000000000001148 ) ) ;
#2378=ORIENTED_EDGE ( 'NONE', *, *, #10013, .T. ) ;
#2405=DIRECTION ( 'NONE',  ( 0.000000000000000000, 0.000000000000000000, 1.000000000000000000 ) ) ;
#2418=EDGE_LOOP ( 'NONE', ( #3030, #5033 ) ) ;
#2426=EDGE_CURVE ( 'NONE', #12637, #11426, #4770, .T. ) ;
#2428=ADVANCED_FACE ( 'NONE', ( #3794, #3550 ), #12505, .T. ) ;
#2436=CIRCLE ( 'NONE', #3738, 0.2000000000000000944 ) ;
#2469=AXIS2_PLACEMENT_3D ( 'NONE', #1218, #4942, #1300 ) ;
#2497=VERTEX_POINT ( 'NONE', #88 ) ;
#2535=DIRECTION ( 'NONE',  ( 0.000000000000000000, 0.000000000000000000, -1.000000000000000000 ) ) ;
#2540=ORIENTED_EDGE ( 'NONE', *, *, #9564, .F. ) ;
#2552=VECTOR ( 'NONE', #2922, 999.9999999999998863 ) ;
#2585=DIRECTION ( 'NONE',  ( 0.000000000000000000, 0.000000000000000000, -1.000000000000000000 ) ) ;
#2609=CARTESIAN_POINT ( 'NONE',  ( 2.500000000000000000, -1.768423874527823569, 1.021000000000002794 ) ) ;
#2623=AXIS2_PLACEMENT_3D ( 'NONE', #11080, #6153, #13469 ) ;
#2641=ORIENTED_EDGE ( 'NONE', *, *, #9390, .T. ) ;
#2646=DIRECTION ( 'NONE',  ( 0.000000000000000000, 0.000000000000000000, 1.000000000000000000 ) ) ;
#2688=CARTESIAN_POINT ( 'NONE',  ( 17.00000000000000000, 0.000000000000000000, 0.000000000000000000 ) ) ;
#2698=CARTESIAN_POINT ( 'NONE',  ( 5.200000000000002842, 3.061616997868383634E-16, -2.500000000000000444 ) ) ;
#2710=DIRECTION ( 'NONE',  ( 0.000000000000000000, 0.000000000000000000, 1.000000000000000000 ) ) ;
#2723=AXIS2_PLACEMENT_3D ( 'NONE', #1059, #15942, #2585 ) ;
#2766=AXIS2_PLACEMENT_3D ( 'NONE', #5472, #10403, #15573 ) ;
#2802=DIRECTION ( 'NONE',  ( 0.000000000000000000, 0.000000000000000000, 1.000000000000000000 ) ) ;
#2814=CARTESIAN_POINT ( 'NONE',  ( 17.00000000000000000, 0.000000000000000000, 0.000000000000000000 ) ) ;
#2818=DIRECTION ( 'NONE',  ( 0.000000000000000000, 1.000000000000000000, -1.471414886128461471E-15 ) ) ;
#2836=DIRECTION ( 'NONE',  ( -1.000000000000000000, -0.000000000000000000, -0.000000000000000000 ) ) ;
#2837=DIRECTION ( 'NONE',  ( 0.000000000000000000, 0.4999999999999993339, -0.8660254037844390407 ) ) ;
#2843=ORIENTED_EDGE ( 'NONE', *, *, #13459, .T. ) ;
#2861=ADVANCED_FACE ( 'NONE', ( #13531 ), #11717, .T. ) ;
#2868=VERTEX_POINT ( 'NONE', #9911 ) ;
#2884=FACE_OUTER_BOUND ( 'NONE', #12556, .T. ) ;
#2899=DIRECTION ( 'NONE',  ( -1.000000000000000000, -0.000000000000000000, -0.000000000000000000 ) ) ;
#2901=DIRECTION ( 'NONE',  ( 1.000000000000000000, 0.000000000000000000, 0.000000000000000000 ) ) ;
#2922=DIRECTION ( 'NONE',  ( 0.000000000000000000, -0.5000000000000012212, -0.8660254037844380415 ) ) ;
#2925=( LENGTH_UNIT ( ) NAMED_UNIT ( * ) SI_UNIT ( .MILLI., .METRE. ) );
#2927=EDGE_CURVE ( 'NONE', #13263, #6259, #15911, .T. ) ;
#2938=ORIENTED_EDGE ( 'NONE', *, *, #8366, .T. ) ;
#2952=CIRCLE ( 'NONE', #131, 2.041999999999999815 ) ;
#2964=AXIS2_PLACEMENT_3D ( 'NONE', #1966, #2049, #9699 ) ;
#3006=AXIS2_PLACEMENT_3D ( 'NONE', #7750, #12644, #8791 ) ;
#3023=ORIENTED_EDGE ( 'NONE', *, *, #780, .T. ) ;
#3030=ORIENTED_EDGE ( 'NONE', *, *, #14261, .F. ) ;
#3086=EDGE_CURVE ( 'NONE', #1929, #3803, #1109, .T. ) ;
#3088=EDGE_CURVE ( 'NONE', #6007, #4880, #12453, .T. ) ;
#3108=DIRECTION ( 'NONE',  ( -1.000000000000000000, -0.000000000000000000, -0.000000000000000000 ) ) ;
#3179=CARTESIAN_POINT ( 'NONE',  ( 2.500000000000000000, 0.000000000000000000, 0.000000000000000000 ) ) ;
#3207=EDGE_LOOP ( 'NONE', ( #10502, #9474, #7054, #6299, #10765 ) ) ;
#3223=AXIS2_PLACEMENT_3D ( 'NONE', #11897, #11972, #4638 ) ;
#3263=LINE ( 'NONE', #15636, #10301 ) ;
#3290=ORIENTED_EDGE ( 'NONE', *, *, #9991, .F. ) ;
#3338=ORIENTED_EDGE ( 'NONE', *, *, #4488, .T. ) ;
#3353=EDGE_LOOP ( 'NONE', ( #1617, #12654, #419, #8201 ) ) ;
#3359=CARTESIAN_POINT ( 'NONE',  ( 2.500000000000000000, 2.357898499370433054, -1.951563910473907981E-15 ) ) ;
#3421=ORIENTED_EDGE ( 'NONE', *, *, #10047, .T. ) ;
#3453=EDGE_LOOP ( 'NONE', ( #1135, #15407 ) ) ;
#3478=CIRCLE ( 'NONE', #2964, 2.500000000000000444 ) ;
#3550=FACE_OUTER_BOUND ( 'NONE', #12172, .T. ) ;
#3574=VECTOR ( 'NONE', #7844, 1000.000000000000114 ) ;
#3582=CIRCLE ( 'NONE', #5660, 4.250000000000000000 ) ;
#3616=DIRECTION ( 'NONE',  ( 0.000000000000000000, -0.5000000000000012212, -0.8660254037844380415 ) ) ;
#3621=ORIENTED_EDGE ( 'NONE', *, *, #2426, .F. ) ;
#3652=SHAPE_DEFINITION_REPRESENTATION ( #10677, #10906 ) ;
#3673=CARTESIAN_POINT ( 'NONE',  ( 5.200000000000002842, 0.000000000000000000, 0.000000000000000000 ) ) ;
#3696=ORIENTED_EDGE ( 'NONE', *, *, #11636, .T. ) ;
#3698=VERTEX_POINT ( 'NONE', #7149 ) ;
#3719=EDGE_CURVE ( 'NONE', #7205, #13141, #10135, .T. ) ;
#3721=PLANE ( 'NONE',  #2723 ) ;
#3738=AXIS2_PLACEMENT_3D ( 'NONE', #10847, #8286, #9481 ) ;
#3743=AXIS2_PLACEMENT_3D ( 'NONE', #2244, #6964, #10667 ) ;
#3769=PLANE ( 'NONE',  #9018 ) ;
#3779=VERTEX_POINT ( 'NONE', #12205 ) ;
#3794=FACE_BOUND ( 'NONE', #6920, .T. ) ;
#3799=CARTESIAN_POINT ( 'NONE',  ( 2.500000000000000000, -1.178949249685213863, 2.042000000000002924 ) ) ;
#3803=VERTEX_POINT ( 'NONE', #107 ) ;
#3834=DIRECTION ( 'NONE',  ( 0.000000000000000000, 0.000000000000000000, 1.000000000000000000 ) ) ;
#3928=LINE ( 'NONE', #8873, #6690 ) ;
#3949=DIRECTION ( 'NONE',  ( 0.000000000000000000, 0.000000000000000000, -1.000000000000000000 ) ) ;
#3953=LINE ( 'NONE', #10353, #7218 ) ;
#3972=VERTEX_POINT ( 'NONE', #13299 ) ;
#3997=FACE_OUTER_BOUND ( 'NONE', #13080, .T. ) ;
#4003=DIRECTION ( 'NONE',  ( 0.000000000000000000, 0.000000000000000000, -1.000000000000000000 ) ) ;
#4006=CARTESIAN_POINT ( 'NONE',  ( 5.000000000000004441, 0.000000000000000000, 0.000000000000000000 ) ) ;
#4021=ORIENTED_EDGE ( 'NONE', *, *, #2927, .T. ) ;
#4049=EDGE_CURVE ( 'NONE', #2497, #4880, #7891, .T. ) ;
#4064=AXIS2_PLACEMENT_3D ( 'NONE', #3673, #9533, #2535 ) ;
#4093=DIRECTION ( 'NONE',  ( 1.000000000000000000, 0.000000000000000000, 0.000000000000000000 ) ) ;
#4111=DIRECTION ( 'NONE',  ( 0.000000000000000000, 0.8660254037844380415, -0.5000000000000011102 ) ) ;
#4134=CARTESIAN_POINT ( 'NONE',  ( 0.000000000000000000, 1.178949249685218525, 2.041999999999999371 ) ) ;
#4145=( NAMED_UNIT ( * ) PLANE_ANGLE_UNIT ( ) SI_UNIT ( $, .RADIAN. ) );
#4155=CARTESIAN_POINT ( 'NONE',  ( -31.74999999999995737, 0.000000000000000000, 2.500000000000000444 ) ) ;
#4190=PLANE ( 'NONE',  #4721 ) ;
#4281=AXIS2_PLACEMENT_3D ( 'NONE', #9847, #13544, #11139 ) ;
#4295=VECTOR ( 'NONE', #14216, 1000.000000000000000 ) ;
#4310=( NAMED_UNIT ( * ) SI_UNIT ( $, .STERADIAN. ) SOLID_ANGLE_UNIT ( ) );
#4330=CIRCLE ( 'NONE', #10531, 4.000000000000000000 ) ;
#4397=DIRECTION ( 'NONE',  ( 0.000000000000000000, 0.000000000000000000, 1.000000000000000000 ) ) ;
#4432=LINE ( 'NONE', #5649, #3574 ) ;
#4488=EDGE_CURVE ( 'NONE', #6791, #7896, #9226, .T. ) ;
#4521=ORIENTED_EDGE ( 'NONE', *, *, #5203, .F. ) ;
#4530=ADVANCED_FACE ( 'NONE', ( #1660 ), #14889, .T. ) ;
#4582=AXIS2_PLACEMENT_3D ( 'NONE', #13894, #8982, #7777 ) ;
#4585=CARTESIAN_POINT ( 'NONE',  ( 2.500000000000000000, 1.768423874527822681, -1.021000000000002794 ) ) ;
#4596=CARTESIAN_POINT ( 'NONE',  ( 17.00000000000000000, 2.055000000000000160, 0.000000000000000000 ) ) ;
#4600=AXIS2_PLACEMENT_3D ( 'NONE', #616, #11820, #771 ) ;
#4636=ORIENTED_EDGE ( 'NONE', *, *, #13750, .F. ) ;
#4638=DIRECTION ( 'NONE',  ( 1.000000000000000000, 0.000000000000000000, 0.000000000000000000 ) ) ;
#4662=PRESENTATION_STYLE_ASSIGNMENT (( #1996 ) ) ;
#4721=AXIS2_PLACEMENT_3D ( 'NONE', #11461, #11383, #7845 ) ;
#4736=( LENGTH_UNIT ( ) NAMED_UNIT ( * ) SI_UNIT ( .MILLI., .METRE. ) );
#4755=DIRECTION ( 'NONE',  ( 1.000000000000000000, 0.000000000000000000, 0.000000000000000000 ) ) ;
#4765=CARTESIAN_POINT ( 'NONE',  ( -31.74999999999995737, 5.204748896376250699E-16, -4.250000000000000000 ) ) ;
#4770=LINE ( 'NONE', #7605, #14501 ) ;
#4842=APPLICATION_CONTEXT ( 'automotive_design' ) ;
#4869=CARTESIAN_POINT ( 'NONE',  ( 0.000000000000000000, -1.178949249685213863, 2.042000000000002924 ) ) ;
#4880=VERTEX_POINT ( 'NONE', #2299 ) ;
#4888=CARTESIAN_POINT ( 'NONE',  ( 2.500000000000000000, -1.178949249685218303, -2.041999999999998039 ) ) ;
#4940=CARTESIAN_POINT ( 'NONE',  ( 0.000000000000000000, 2.357898499370433054, -1.951563910473907981E-15 ) ) ;
#4942=DIRECTION ( 'NONE',  ( -1.000000000000000000, -0.000000000000000000, -0.000000000000000000 ) ) ;
#4957=FACE_OUTER_BOUND ( 'NONE', #12642, .T. ) ;
#5009=STYLED_ITEM ( 'NONE', ( #4662 ), #5806 ) ;
#5033=ORIENTED_EDGE ( 'NONE', *, *, #11796, .F. ) ;
#5106=VECTOR ( 'NONE', #2899, 1000.000000000000000 ) ;
#5109=VECTOR ( 'NONE', #13686, 1000.000000000000000 ) ;
#5114=EDGE_CURVE ( 'NONE', #12637, #6791, #12545, .T. ) ;
#5116=ORIENTED_EDGE ( 'NONE', *, *, #15078, .T. ) ;
#5119=AXIS2_PLACEMENT_3D ( 'NONE', #12872, #11585, #15242 ) ;
#5129=AXIS2_PLACEMENT_3D ( 'NONE', #7483, #9975, #3834 ) ;
#5154=CARTESIAN_POINT ( 'NONE',  ( 2.500000000000000000, 0.000000000000000000, 0.000000000000000000 ) ) ;
#5203=EDGE_CURVE ( 'NONE', #11426, #7997, #13585, .T. ) ;
#5217=ORIENTED_EDGE ( 'NONE', *, *, #5114, .F. ) ;
#5260=ORIENTED_EDGE ( 'NONE', *, *, #8366, .F. ) ;
#5306=LINE ( 'NONE', #11287, #1092 ) ;
#5307=DIRECTION ( 'NONE',  ( 0.000000000000000000, 0.000000000000000000, 1.000000000000000000 ) ) ;
#5345=ADVANCED_FACE ( 'NONE', ( #15420 ), #7694, .F. ) ;
#5368=PRESENTATION_STYLE_ASSIGNMENT (( #14087 ) ) ;
#5396=DIRECTION ( 'NONE',  ( 0.000000000000000000, 0.000000000000000000, -1.000000000000000000 ) ) ;
#5400=AXIS2_PLACEMENT_3D ( 'NONE', #5720, #4111, #9059 ) ;
#5472=CARTESIAN_POINT ( 'NONE',  ( 5.200000000000002842, 0.000000000000000000, 0.000000000000000000 ) ) ;
#5559=ORIENTED_EDGE ( 'NONE', *, *, #7377, .F. ) ;
#5598=VERTEX_POINT ( 'NONE', #4134 ) ;
#5602=ORIENTED_EDGE ( 'NONE', *, *, #5827, .T. ) ;
#5605=SURFACE_STYLE_FILL_AREA ( #10381 ) ;
#5610=EDGE_CURVE ( 'NONE', #12513, #3779, #8281, .T. ) ;
#5623=DIRECTION ( 'NONE',  ( 0.000000000000000000, 1.000000000000000000, -1.287488025362403787E-15 ) ) ;
#5632=VECTOR ( 'NONE', #9, 1000.000000000000000 ) ;
#5635=LINE ( 'NONE', #10578, #15704 ) ;
#5639=UNCERTAINTY_MEASURE_WITH_UNIT (LENGTH_MEASURE( 1.000000000000000082E-05 ), #2925, 'distance_accuracy_value', 'NONE');
#5649=CARTESIAN_POINT ( 'NONE',  ( 0.000000000000000000, 2.357898499370433054, -1.951563910473907981E-15 ) ) ;
#5660=AXIS2_PLACEMENT_3D ( 'NONE', #5966, #9668, #5307 ) ;
#5679=ORIENTED_EDGE ( 'NONE', *, *, #14762, .T. ) ;
#5720=CARTESIAN_POINT ( 'NONE',  ( 2.500000000000000000, -1.178949249685213863, 2.042000000000002924 ) ) ;
#5806=ADVANCED_BREP_SHAPE_REPRESENTATION ( '', ( #14097, #3223 ), #7865 ) ;
#5819=VECTOR ( 'NONE', #6159, 1000.000000000000000 ) ;
#5827=EDGE_CURVE ( 'NONE', #4880, #6007, #15949, .T. ) ;
#5864=EDGE_CURVE ( 'NONE', #13141, #1955, #4330, .T. ) ;
#5875=( NAMED_UNIT ( * ) PLANE_ANGLE_UNIT ( ) SI_UNIT ( $, .RADIAN. ) );
#5883=CARTESIAN_POINT ( 'NONE',  ( 5.000000000000002665, 3.306546357697854226E-16, 2.700000000000000622 ) ) ;
#5899=CYLINDRICAL_SURFACE ( 'NONE', #4281, 4.250000000000000000 ) ;
#5905=EDGE_CURVE ( 'NONE', #2868, #3779, #10233, .T. ) ;
#5966=CARTESIAN_POINT ( 'NONE',  ( 0.2500000000000002220, 0.000000000000000000, 0.000000000000000000 ) ) ;
#5968=CARTESIAN_POINT ( 'NONE',  ( 0.2500000000000002220, 0.000000000000000000, 0.000000000000000000 ) ) ;
#5998=AXIS2_PLACEMENT_3D ( 'NONE', #11015, #7070, #997 ) ;
#6007=VERTEX_POINT ( 'NONE', #2698 ) ;
#6020=AXIS2_PLACEMENT_3D ( 'NONE', #10249, #4093, #5396 ) ;
#6052=ORIENTED_EDGE ( 'NONE', *, *, #13497, .T. ) ;
#6092=CARTESIAN_POINT ( 'NONE',  ( 2.500000000000000000, 2.357898499370433054, -1.951563910473907981E-15 ) ) ;
#6118=ORIENTED_EDGE ( 'NONE', *, *, #9075, .F. ) ;
#6138=EDGE_LOOP ( 'NONE', ( #13352, #7956, #4521 ) ) ;
#6147=EDGE_CURVE ( 'NONE', #7997, #13263, #14660, .T. ) ;
#6153=DIRECTION ( 'NONE',  ( -1.000000000000000000, 0.000000000000000000, -0.000000000000000000 ) ) ;
#6159=DIRECTION ( 'NONE',  ( -1.000000000000000000, -0.000000000000000000, -0.000000000000000000 ) ) ;
#6191=CYLINDRICAL_SURFACE ( 'NONE', #5129, 2.500000000000000444 ) ;
#6255=EDGE_CURVE ( 'NONE', #6259, #3698, #12291, .T. ) ;
#6259=VERTEX_POINT ( 'NONE', #1146 ) ;
#6262=DIRECTION ( 'NONE',  ( 0.000000000000000000, 0.000000000000000000, -1.000000000000000000 ) ) ;
#6298=ORIENTED_EDGE ( 'NONE', *, *, #6525, .T. ) ;
#6299=ORIENTED_EDGE ( 'NONE', *, *, #13497, .F. ) ;
#6308=CARTESIAN_POINT ( 'NONE',  ( -31.74999999999995737, 0.000000000000000000, 0.000000000000000000 ) ) ;
#6326=AXIS2_PLACEMENT_3D ( 'NONE', #7102, #8555, #1098 ) ;
#6338=COLOUR_RGB ( '', 0.40784314, 0.44705882, 0.49803922) ;
#6342=AXIS2_PLACEMENT_3D ( 'NONE', #9535, #14385, #10977 ) ;
#6343=DIRECTION ( 'NONE',  ( -1.000000000000000000, -0.000000000000000000, -0.000000000000000000 ) ) ;
#6370=DIRECTION ( 'NONE',  ( -0.000000000000000000, 0.8660254037844390407, 0.4999999999999993339 ) ) ;
#6382=ADVANCED_FACE ( 'NONE', ( #11971 ), #924, .T. ) ;
#6453=DIRECTION ( 'NONE',  ( 0.000000000000000000, -0.4999999999999992784, 0.8660254037844389297 ) ) ;
#6503=PLANE ( 'NONE',  #13028 ) ;
#6525=EDGE_CURVE ( 'NONE', #3803, #7205, #14785, .T. ) ;
#6533=ORIENTED_EDGE ( 'NONE', *, *, #10047, .F. ) ;
#6544=PLANE ( 'NONE',  #8102 ) ;
#6549=LINE ( 'NONE', #1608, #5106 ) ;
#6579=FACE_OUTER_BOUND ( 'NONE', #14060, .T. ) ;
#6592=ORIENTED_EDGE ( 'NONE', *, *, #1796, .T. ) ;
#6658=ORIENTED_EDGE ( 'NONE', *, *, #1796, .F. ) ;
#6662=DIRECTION ( 'NONE',  ( -0.7071067811865369146, 8.659560562355062281E-17, -0.7071067811865582309 ) ) ;
#6679=EDGE_LOOP ( 'NONE', ( #4021, #6052, #3290 ) ) ;
#6684=ORIENTED_EDGE ( 'NONE', *, *, #888, .T. ) ;
#6690=VECTOR ( 'NONE', #7669, 1000.000000000000000 ) ;
#6698=CONICAL_SURFACE ( 'NONE', #12829, 2.041999999999999815, 1.047197551196591858 ) ;
#6707=VERTEX_POINT ( 'NONE', #4888 ) ;
#6730=VERTEX_POINT ( 'NONE', #2609 ) ;
#6765=DIRECTION ( 'NONE',  ( 0.000000000000000000, 0.000000000000000000, 1.000000000000000000 ) ) ;
#6776=ORIENTED_EDGE ( 'NONE', *, *, #6147, .T. ) ;
#6782=DIRECTION ( 'NONE',  ( 0.000000000000000000, 0.000000000000000000, 1.000000000000000000 ) ) ;
#6791=VERTEX_POINT ( 'NONE', #12217 ) ;
#6827=ORIENTED_EDGE ( 'NONE', *, *, #3719, .T. ) ;
#6838=ADVANCED_FACE ( 'NONE', ( #6579 ), #2288, .T. ) ;
#6865=DIRECTION ( 'NONE',  ( -1.000000000000000000, -0.000000000000000000, -0.000000000000000000 ) ) ;
#6875=ORIENTED_EDGE ( 'NONE', *, *, #10758, .F. ) ;
#6918=ORIENTED_EDGE ( 'NONE', *, *, #13326, .T. ) ;
#6920=EDGE_LOOP ( 'NONE', ( #2378, #8318, #11294, #15860, #10789, #11900 ) ) ;
#6951=FACE_OUTER_BOUND ( 'NONE', #13877, .T. ) ;
#6964=DIRECTION ( 'NONE',  ( -1.000000000000000000, -0.000000000000000000, -0.000000000000000000 ) ) ;
#6966=ORIENTED_EDGE ( 'NONE', *, *, #2426, .T. ) ;
#7019=( NAMED_UNIT ( * ) SI_UNIT ( $, .STERADIAN. ) SOLID_ANGLE_UNIT ( ) );
#7023=DIRECTION ( 'NONE',  ( 0.000000000000000000, -0.4999999999999993894, 0.8660254037844389297 ) ) ;
#7039=LINE ( 'NONE', #2017, #14433 ) ;
#7054=ORIENTED_EDGE ( 'NONE', *, *, #14232, .F. ) ;
#7061=LINE ( 'NONE', #14559, #11984 ) ;
#7070=DIRECTION ( 'NONE',  ( -0.000000000000000000, 1.000000000000000000, 1.224646799147353207E-16 ) ) ;
#7102=CARTESIAN_POINT ( 'NONE',  ( 5.200000000000002842, 0.000000000000000000, -2.700000000000000622 ) ) ;
#7149=CARTESIAN_POINT ( 'NONE',  ( 0.000000000000000000, 1.178949249685213863, -2.042000000000001148 ) ) ;
#7168=PLANE ( 'NONE',  #511 ) ;
#7205=VERTEX_POINT ( 'NONE', #9871 ) ;
#7218=VECTOR ( 'NONE', #15280, 1000.000000000000000 ) ;
#7246=CARTESIAN_POINT ( 'NONE',  ( 0.000000000000000000, 0.000000000000000000, 4.000000000000000000 ) ) ;
#7299=AXIS2_PLACEMENT_3D ( 'NONE', #10108, #12832, #15282 ) ;
#7321=FACE_OUTER_BOUND ( 'NONE', #9289, .T. ) ;
#7343=ORIENTED_EDGE ( 'NONE', *, *, #3088, .F. ) ;
#7366=LINE ( 'NONE', #14795, #5819 ) ;
#7372=CARTESIAN_POINT ( 'NONE',  ( 3.678949249685231848, 5.299604027854762026E-17, 0.000000000000000000 ) ) ;
#7377=EDGE_CURVE ( 'NONE', #11041, #7205, #3582, .T. ) ;
#7421=CARTESIAN_POINT ( 'NONE',  ( 2.500000000000000000, 1.178949249685218525, 2.041999999999999371 ) ) ;
#7422=ADVANCED_FACE ( 'NONE', ( #14937 ), #3769, .T. ) ;
#7469=DIRECTION ( 'NONE',  ( 0.000000000000000000, -0.5000000000000011102, -0.8660254037844379305 ) ) ;
#7483=CARTESIAN_POINT ( 'NONE',  ( -31.74999999999995737, 0.000000000000000000, 0.000000000000000000 ) ) ;
#7524=CYLINDRICAL_SURFACE ( 'NONE', #10150, 2.500000000000000444 ) ;
#7555=EDGE_CURVE ( 'NONE', #1929, #11041, #8715, .T. ) ;
#7586=EDGE_CURVE ( 'NONE', #11426, #1698, #3928, .T. ) ;
#7605=CARTESIAN_POINT ( 'NONE',  ( 2.500000000000000000, 0.000000000000000000, 2.041999999999999815 ) ) ;
#7639=CIRCLE ( 'NONE', #13526, 2.055000000000000160 ) ;
#7659=ORIENTED_EDGE ( 'NONE', *, *, #3719, .F. ) ;
#7669=DIRECTION ( 'NONE',  ( 0.000000000000000000, 1.000000000000000000, -1.471414886128461471E-15 ) ) ;
#7694=TOROIDAL_SURFACE ( 'NONE', #2766, 2.700000000000000622, 0.2000000000000000111 ) ;
#7714=PRODUCT_CONTEXT ( 'NONE', #4842, 'mechanical' ) ;
#7718=EDGE_LOOP ( 'NONE', ( #13394, #5260, #9602, #6918, #11759 ) ) ;
#7742=CARTESIAN_POINT ( 'NONE',  ( 0.000000000000000000, 0.000000000000000000, 0.000000000000000000 ) ) ;
#7750=CARTESIAN_POINT ( 'NONE',  ( 2.500000000000000000, -1.178949249685213863, 2.042000000000002924 ) ) ;
#7770=VERTEX_POINT ( 'NONE', #11911 ) ;
#7774=FACE_OUTER_BOUND ( 'NONE', #2267, .T. ) ;
#7777=DIRECTION ( 'NONE',  ( 0.000000000000000000, 0.000000000000000000, -1.000000000000000000 ) ) ;
#7788=DIRECTION ( 'NONE',  ( 0.000000000000000000, 0.000000000000000000, 1.000000000000000000 ) ) ;
#7833=ADVANCED_FACE ( 'NONE', ( #10719 ), #7168, .F. ) ;
#7837=VERTEX_POINT ( 'NONE', #12220 ) ;
#7844=DIRECTION ( 'NONE',  ( 0.000000000000000000, -0.4999999999999993894, 0.8660254037844389297 ) ) ;
#7845=DIRECTION ( 'NONE',  ( 0.000000000000000000, 0.5000000000000012212, 0.8660254037844380415 ) ) ;
#7852=DIRECTION ( 'NONE',  ( 0.000000000000000000, 0.000000000000000000, 1.000000000000000000 ) ) ;
#7865=( GEOMETRIC_REPRESENTATION_CONTEXT ( 3 ) GLOBAL_UNCERTAINTY_ASSIGNED_CONTEXT ( ( #7883 ) ) GLOBAL_UNIT_ASSIGNED_CONTEXT ( ( #10114, #8080, #12975 ) ) REPRESENTATION_CONTEXT ( 'NONE', 'WORKASPACE' ) );
#7883=UNCERTAINTY_MEASURE_WITH_UNIT (LENGTH_MEASURE( 1.000000000000000082E-05 ), #10114, 'distance_accuracy_value', 'NONE');
#7891=LINE ( 'NONE', #4155, #12022 ) ;
#7896=VERTEX_POINT ( 'NONE', #15888 ) ;
#7913=ORIENTED_EDGE ( 'NONE', *, *, #9991, .T. ) ;
#7956=ORIENTED_EDGE ( 'NONE', *, *, #13326, .F. ) ;
#7957=LINE ( 'NONE', #9010, #8738 ) ;
#7997=VERTEX_POINT ( 'NONE', #10066 ) ;
#8023=ADVANCED_FACE ( 'NONE', ( #11345 ), #6191, .T. ) ;
#8080=( NAMED_UNIT ( * ) PLANE_ANGLE_UNIT ( ) SI_UNIT ( $, .RADIAN. ) );
#8086=AXIS2_PLACEMENT_3D ( 'NONE', #9115, #15086, #4003 ) ;
#8102=AXIS2_PLACEMENT_3D ( 'NONE', #1605, #10102, #3949 ) ;
#8122=EDGE_CURVE ( 'NONE', #3803, #1929, #15446, .T. ) ;
#8167=CONICAL_SURFACE ( 'NONE', #13051, 2.041999999999999815, 1.047197551196591858 ) ;
#8201=ORIENTED_EDGE ( 'NONE', *, *, #13459, .F. ) ;
#8221=VECTOR ( 'NONE', #13171, 1000.000000000000114 ) ;
#8225=DIRECTION ( 'NONE',  ( -1.000000000000000000, -0.000000000000000000, -0.000000000000000000 ) ) ;
#8231=AXIS2_PLACEMENT_3D ( 'NONE', #15725, #8450, #12133 ) ;
#8270=CARTESIAN_POINT ( 'NONE',  ( -31.74999999999995737, 0.000000000000000000, 0.000000000000000000 ) ) ;
#8281=LINE ( 'NONE', #904, #8221 ) ;
#8286=DIRECTION ( 'NONE',  ( 0.000000000000000000, 1.000000000000000000, -1.224646799147353207E-16 ) ) ;
#8294=DIRECTION ( 'NONE',  ( 0.000000000000000000, 0.4999999999999993339, -0.8660254037844390407 ) ) ;
#8298=ORIENTED_EDGE ( 'NONE', *, *, #10758, .T. ) ;
#8302=PLANE ( 'NONE',  #12710 ) ;
#8309=DIRECTION ( 'NONE',  ( 0.000000000000000000, 0.000000000000000000, -1.000000000000000000 ) ) ;
#8318=ORIENTED_EDGE ( 'NONE', *, *, #9855, .F. ) ;
#8346=DIRECTION ( 'NONE',  ( -1.000000000000000000, -0.000000000000000000, -0.000000000000000000 ) ) ;
#8357=AXIS2_PLACEMENT_3D ( 'NONE', #4006, #13870, #2802 ) ;
#8359=DIRECTION ( 'NONE',  ( 0.000000000000000000, 0.000000000000000000, 1.000000000000000000 ) ) ;
#8366=EDGE_CURVE ( 'NONE', #14589, #12457, #3953, .T. ) ;
#8392=ORIENTED_EDGE ( 'NONE', *, *, #10732, .F. ) ;
#8416=ADVANCED_FACE ( 'NONE', ( #12429 ), #6698, .F. ) ;
#8420=ORIENTED_EDGE ( 'NONE', *, *, #5114, .T. ) ;
#8437=AXIS2_PLACEMENT_3D ( 'NONE', #2814, #13713, #2646 ) ;
#8450=DIRECTION ( 'NONE',  ( 0.000000000000000000, -0.8660254037844390407, -0.4999999999999994449 ) ) ;
#8453=AXIS2_PLACEMENT_3D ( 'NONE', #5154, #13698, #2710 ) ;
#8455=ORIENTED_EDGE ( 'NONE', *, *, #8484, .F. ) ;
#8457=VECTOR ( 'NONE', #13700, 1000.000000000000000 ) ;
#8465=ADVANCED_FACE ( 'NONE', ( #15038 ), #8897, .F. ) ;
#8484=EDGE_CURVE ( 'NONE', #1698, #5598, #6549, .T. ) ;
#8545=DIRECTION ( 'NONE',  ( -1.000000000000000000, -0.000000000000000000, -0.000000000000000000 ) ) ;
#8550=ORIENTED_EDGE ( 'NONE', *, *, #12160, .F. ) ;
#8555=DIRECTION ( 'NONE',  ( 0.000000000000000000, -1.000000000000000000, 0.000000000000000000 ) ) ;
#8567=ORIENTED_EDGE ( 'NONE', *, *, #12775, .F. ) ;
#8591=CARTESIAN_POINT ( 'NONE',  ( 0.000000000000000000, 2.357898499370433054, -1.951563910473907981E-15 ) ) ;
#8594=CIRCLE ( 'NONE', #14523, 4.250000000000000000 ) ;
#8600=EDGE_LOOP ( 'NONE', ( #12596, #8882, #2641, #6684, #5679 ) ) ;
#8713=DIRECTION ( 'NONE',  ( 0.000000000000000000, 0.000000000000000000, 1.000000000000000000 ) ) ;
#8715=LINE ( 'NONE', #148, #8457 ) ;
#8724=ORIENTED_EDGE ( 'NONE', *, *, #6525, .F. ) ;
#8738=VECTOR ( 'NONE', #6662, 1000.000000000000000 ) ;
#8744=DIRECTION ( 'NONE',  ( 0.000000000000000000, 1.000000000000000000, -1.471414886128461471E-15 ) ) ;
#8787=ORIENTED_EDGE ( 'NONE', *, *, #22, .F. ) ;
#8791=DIRECTION ( 'NONE',  ( 0.000000000000000000, -1.000000000000000000, 1.471414886128461471E-15 ) ) ;
#8795=FACE_OUTER_BOUND ( 'NONE', #14699, .T. ) ;
#8871=CARTESIAN_POINT ( 'NONE',  ( 0.2500000000000002220, 0.000000000000000000, 0.000000000000000000 ) ) ;
#8873=CARTESIAN_POINT ( 'NONE',  ( 2.500000000000000000, -1.178949249685213863, 2.042000000000002924 ) ) ;
#8882=ORIENTED_EDGE ( 'NONE', *, *, #5905, .F. ) ;
#8897=PLANE ( 'NONE',  #4582 ) ;
#8929=EDGE_LOOP ( 'NONE', ( #6533, #9658, #4636 ) ) ;
#8982=DIRECTION ( 'NONE',  ( 1.000000000000000000, 0.000000000000000000, 0.000000000000000000 ) ) ;
#9004=AXIS2_PLACEMENT_3D ( 'NONE', #9579, #8545, #14510 ) ;
#9010=CARTESIAN_POINT ( 'NONE',  ( 17.00000000000000000, 2.516649172247811061E-16, -2.055000000000000160 ) ) ;
#9018=AXIS2_PLACEMENT_3D ( 'NONE', #10163, #6370, #6453 ) ;
#9059=DIRECTION ( 'NONE',  ( 0.000000000000000000, 0.5000000000000011102, 0.8660254037844380415 ) ) ;
#9065=DIRECTION ( 'NONE',  ( -1.000000000000000000, -0.000000000000000000, -0.000000000000000000 ) ) ;
#9075=EDGE_CURVE ( 'NONE', #7770, #12513, #5635, .T. ) ;
#9115=CARTESIAN_POINT ( 'NONE',  ( 5.000000000000000888, 4.250000000000000000, 0.000000000000000000 ) ) ;
#9127=ADVANCED_FACE ( 'NONE', ( #7321 ), #15424, .T. ) ;
#9134=CARTESIAN_POINT ( 'NONE',  ( 2.500000000000000000, 0.000000000000000000, 0.000000000000000000 ) ) ;
#9226=CIRCLE ( 'NONE', #8453, 2.041999999999999815 ) ;
#9228=EDGE_LOOP ( 'NONE', ( #9410, #7343, #2843, #12177 ) ) ;
#9289=EDGE_LOOP ( 'NONE', ( #8392, #9456, #3696, #8567 ) ) ;
#9311=CYLINDRICAL_SURFACE ( 'NONE', #15124, 4.250000000000000000 ) ;
#9335=VERTEX_POINT ( 'NONE', #12705 ) ;
#9342=EDGE_LOOP ( 'NONE', ( #948, #6298, #3023, #10787 ) ) ;
#9352=ADVANCED_FACE ( 'NONE', ( #12782 ), #11732, .F. ) ;
#9384=FACE_OUTER_BOUND ( 'NONE', #11236, .T. ) ;
#9390=EDGE_CURVE ( 'NONE', #2868, #7896, #3263, .T. ) ;
#9402=SURFACE_SIDE_STYLE ('',( #5605 ) ) ;
#9410=ORIENTED_EDGE ( 'NONE', *, *, #14245, .F. ) ;
#9437=FILL_AREA_STYLE ('',( #10653 ) ) ;
#9440=LINE ( 'NONE', #1834, #4295 ) ;
#9456=ORIENTED_EDGE ( 'NONE', *, *, #11796, .T. ) ;
#9474=ORIENTED_EDGE ( 'NONE', *, *, #14762, .F. ) ;
#9481=DIRECTION ( 'NONE',  ( 0.000000000000000000, 1.224646799147353207E-16, 1.000000000000000000 ) ) ;
#9489=ORIENTED_EDGE ( 'NONE', *, *, #5610, .F. ) ;
#9533=DIRECTION ( 'NONE',  ( 1.000000000000000000, 0.000000000000000000, 0.000000000000000000 ) ) ;
#9535=CARTESIAN_POINT ( 'NONE',  ( 5.200000000000002842, 0.000000000000000000, 0.000000000000000000 ) ) ;
#9540=DIRECTION ( 'NONE',  ( 0.000000000000000000, 0.000000000000000000, 1.000000000000000000 ) ) ;
#9564=EDGE_CURVE ( 'NONE', #6730, #2868, #10125, .T. ) ;
#9579=CARTESIAN_POINT ( 'NONE',  ( 17.00000000000000000, 0.000000000000000000, 0.000000000000000000 ) ) ;
#9602=ORIENTED_EDGE ( 'NONE', *, *, #22, .T. ) ;
#9657=ORIENTED_EDGE ( 'NONE', *, *, #14261, .T. ) ;
#9658=ORIENTED_EDGE ( 'NONE', *, *, #656, .T. ) ;
#9668=DIRECTION ( 'NONE',  ( 1.000000000000000000, 0.000000000000000000, 0.000000000000000000 ) ) ;
#9699=DIRECTION ( 'NONE',  ( 0.000000000000000000, 0.000000000000000000, 1.000000000000000000 ) ) ;
#9723=LINE ( 'NONE', #6092, #14627 ) ;
#9751=VECTOR ( 'NONE', #9805, 1000.000000000000000 ) ;
#9795=LINE ( 'NONE', #4940, #12362 ) ;
#9805=DIRECTION ( 'NONE',  ( -1.000000000000000000, -0.000000000000000000, -0.000000000000000000 ) ) ;
#9847=CARTESIAN_POINT ( 'NONE',  ( -31.74999999999995737, 0.000000000000000000, 0.000000000000000000 ) ) ;
#9855=EDGE_CURVE ( 'NONE', #12513, #5598, #12663, .T. ) ;
#9871=CARTESIAN_POINT ( 'NONE',  ( 0.2500000000000002220, 5.204748896376250699E-16, -4.250000000000000000 ) ) ;
#9872=CIRCLE ( 'NONE', #7299, 0.2500000000000002220 ) ;
#9879=VECTOR ( 'NONE', #3616, 999.9999999999998863 ) ;
#9901=ORIENTED_EDGE ( 'NONE', *, *, #656, .F. ) ;
#9906=DIRECTION ( 'NONE',  ( -1.000000000000000000, -0.000000000000000000, -0.000000000000000000 ) ) ;
#9911=CARTESIAN_POINT ( 'NONE',  ( 2.500000000000000000, -2.357898499370432610, 3.252606517456513302E-15 ) ) ;
#9924=FACE_OUTER_BOUND ( 'NONE', #9342, .T. ) ;
#9926=ORIENTED_EDGE ( 'NONE', *, *, #2927, .F. ) ;
#9937=( GEOMETRIC_REPRESENTATION_CONTEXT ( 3 ) GLOBAL_UNCERTAINTY_ASSIGNED_CONTEXT ( ( #5639 ) ) GLOBAL_UNIT_ASSIGNED_CONTEXT ( ( #2925, #4145, #4310 ) ) REPRESENTATION_CONTEXT ( 'NONE', 'WORKASPACE' ) );
#9944=CARTESIAN_POINT ( 'NONE',  ( 0.2500000000000002220, 0.000000000000000000, 4.250000000000000000 ) ) ;
#9946=CIRCLE ( 'NONE', #3743, 2.041999999999999815 ) ;
#9947=ORIENTED_EDGE ( 'NONE', *, *, #5905, .T. ) ;
#9975=DIRECTION ( 'NONE',  ( -1.000000000000000000, -0.000000000000000000, -0.000000000000000000 ) ) ;
#9991=EDGE_CURVE ( 'NONE', #13263, #6791, #15470, .T. ) ;
#10013=EDGE_CURVE ( 'NONE', #12457, #5598, #4432, .T. ) ;
#10016=ORIENTED_EDGE ( 'NONE', *, *, #15078, .F. ) ;
#10045=ADVANCED_FACE ( 'NONE', ( #6951 ), #11852, .T. ) ;
#10047=EDGE_CURVE ( 'NONE', #7770, #6730, #7039, .T. ) ;
#10060=CARTESIAN_POINT ( 'NONE',  ( 2.500000000000000000, 2.357898499370433054, -1.951563910473907981E-15 ) ) ;
#10066=CARTESIAN_POINT ( 'NONE',  ( 2.500000000000000000, 1.768423874527824902, 1.020999999999999019 ) ) ;
#10082=DIRECTION ( 'NONE',  ( 0.000000000000000000, -1.000000000000000000, 1.287488025362403787E-15 ) ) ;
#10086=EDGE_CURVE ( 'NONE', #3779, #7837, #740, .T. ) ;
#10102=DIRECTION ( 'NONE',  ( 1.000000000000000000, 0.000000000000000000, 0.000000000000000000 ) ) ;
#10108=CARTESIAN_POINT ( 'NONE',  ( 0.2500000000000002220, 0.000000000000000000, 4.000000000000000000 ) ) ;
#10114=( LENGTH_UNIT ( ) NAMED_UNIT ( * ) SI_UNIT ( .MILLI., .METRE. ) );
#10125=LINE ( 'NONE', #14734, #14665 ) ;
#10135=CIRCLE ( 'NONE', #5998, 0.2500000000000002220 ) ;
#10150=AXIS2_PLACEMENT_3D ( 'NONE', #6308, #13643, #2405 ) ;
#10163=CARTESIAN_POINT ( 'NONE',  ( 2.500000000000000000, -2.357898499370432610, 3.252606517456513302E-15 ) ) ;
#10225=VECTOR ( 'NONE', #7023, 1000.000000000000114 ) ;
#10233=LINE ( 'NONE', #14010, #5109 ) ;
#10245=DIRECTION ( 'NONE',  ( -1.000000000000000000, -0.000000000000000000, -0.000000000000000000 ) ) ;
#10249=CARTESIAN_POINT ( 'NONE',  ( 5.200000000000002842, 0.000000000000000000, 0.000000000000000000 ) ) ;
#10301=VECTOR ( 'NONE', #8294, 1000.000000000000000 ) ;
#10310=VECTOR ( 'NONE', #2818, 1000.000000000000000 ) ;
#10353=CARTESIAN_POINT ( 'NONE',  ( 2.500000000000000000, 2.357898499370433054, -1.951563910473907981E-15 ) ) ;
#10381=FILL_AREA_STYLE ('',( #14252 ) ) ;
#10403=DIRECTION ( 'NONE',  ( 1.000000000000000000, 0.000000000000000000, 0.000000000000000000 ) ) ;
#10417=CARTESIAN_POINT ( 'NONE',  ( 2.500000000000000000, 2.357898499370433054, -1.951563910473907981E-15 ) ) ;
#10435=DIRECTION ( 'NONE',  ( -1.000000000000000000, -0.000000000000000000, -0.000000000000000000 ) ) ;
#10466=VERTEX_POINT ( 'NONE', #13262 ) ;
#10502=ORIENTED_EDGE ( 'NONE', *, *, #11885, .T. ) ;
#10531=AXIS2_PLACEMENT_3D ( 'NONE', #7742, #220, #12553 ) ;
#10565=FACE_OUTER_BOUND ( 'NONE', #3207, .T. ) ;
#10568=AXIS2_PLACEMENT_3D ( 'NONE', #9134, #6865, #6782 ) ;
#10578=CARTESIAN_POINT ( 'NONE',  ( 2.500000000000000000, -1.178949249685213863, 2.042000000000002924 ) ) ;
#10653=FILL_AREA_STYLE_COLOUR ( '', #894 ) ;
#10656=LINE ( 'NONE', #10417, #10225 ) ;
#10667=DIRECTION ( 'NONE',  ( 0.000000000000000000, 0.000000000000000000, 1.000000000000000000 ) ) ;
#10677=PRODUCT_DEFINITION_SHAPE ( 'NONE', 'NONE',  #501 ) ;
#10719=FACE_OUTER_BOUND ( 'NONE', #8929, .T. ) ;
#10732=EDGE_CURVE ( 'NONE', #10466, #15821, #7957, .T. ) ;
#10754=CIRCLE ( 'NONE', #13565, 4.000000000000000000 ) ;
#10758=EDGE_CURVE ( 'NONE', #14589, #13263, #12770, .T. ) ;
#10765=ORIENTED_EDGE ( 'NONE', *, *, #6255, .T. ) ;
#10787=ORIENTED_EDGE ( 'NONE', *, *, #7555, .F. ) ;
#10789=ORIENTED_EDGE ( 'NONE', *, *, #11885, .F. ) ;
#10847=CARTESIAN_POINT ( 'NONE',  ( 5.200000000000002842, 3.306546357697854226E-16, 2.700000000000000622 ) ) ;
#10867=DIRECTION ( 'NONE',  ( 1.000000000000000000, 0.000000000000000000, 0.000000000000000000 ) ) ;
#10906=SHAPE_REPRESENTATION ( 'socket head cap screw_iso_ISO 4762 M5 x 12 - 12N', ( #3223 ), #7865 ) ;
#10909=DIRECTION ( 'NONE',  ( -0.5000000000000051070, 0.000000000000000000, 0.8660254037844355990 ) ) ;
#10977=DIRECTION ( 'NONE',  ( 0.000000000000000000, 0.000000000000000000, -1.000000000000000000 ) ) ;
#10983=CARTESIAN_POINT ( 'NONE',  ( 2.500000000000000000, 3.004629197474318851E-15, 2.042000000000000259 ) ) ;
#11015=CARTESIAN_POINT ( 'NONE',  ( 0.2500000000000002220, 4.898587196589412829E-16, -4.000000000000000000 ) ) ;
#11025=EDGE_CURVE ( 'NONE', #12457, #3698, #9795, .T. ) ;
#11041=VERTEX_POINT ( 'NONE', #9944 ) ;
#11070=ADVANCED_FACE ( 'NONE', ( #12123 ), #3721, .F. ) ;
#11080=CARTESIAN_POINT ( 'NONE',  ( 0.000000000000000000, 0.000000000000000000, 0.000000000000000000 ) ) ;
#11139=DIRECTION ( 'NONE',  ( 0.000000000000000000, 0.000000000000000000, 1.000000000000000000 ) ) ;
#11199=MECHANICAL_DESIGN_GEOMETRIC_PRESENTATION_REPRESENTATION('',(#5009),#1137);
#11201=FACE_BOUND ( 'NONE', #3453, .T. ) ;
#11236=EDGE_LOOP ( 'NONE', ( #8724, #1892, #1911, #15226 ) ) ;
#11239=ORIENTED_EDGE ( 'NONE', *, *, #5203, .T. ) ;
#11287=CARTESIAN_POINT ( 'NONE',  ( -31.74999999999995737, 3.061616997868383634E-16, -2.500000000000000444 ) ) ;
#11294=ORIENTED_EDGE ( 'NONE', *, *, #5610, .T. ) ;
#11326=AXIS2_PLACEMENT_3D ( 'NONE', #2688, #6343, #11580 ) ;
#11345=FACE_OUTER_BOUND ( 'NONE', #14797, .T. ) ;
#11349=ADVANCED_FACE ( 'NONE', ( #9384 ), #9311, .T. ) ;
#11383=DIRECTION ( 'NONE',  ( 0.000000000000000000, 0.8660254037844380415, -0.5000000000000012212 ) ) ;
#11426=VERTEX_POINT ( 'NONE', #10983 ) ;
#11458=ADVANCED_FACE ( 'NONE', ( #9924 ), #5899, .T. ) ;
#11461=CARTESIAN_POINT ( 'NONE',  ( 2.500000000000000000, 2.357898499370433054, -1.951563910473907981E-15 ) ) ;
#11480=MECHANICAL_DESIGN_GEOMETRIC_PRESENTATION_REPRESENTATION('',(#1420),#9937);
#11511=ORIENTED_EDGE ( 'NONE', *, *, #780, .F. ) ;
#11537=CARTESIAN_POINT ( 'NONE',  ( 0.000000000000000000, 5.051668046482832750E-16, -4.000000000000000000 ) ) ;
#11580=DIRECTION ( 'NONE',  ( 0.000000000000000000, 0.000000000000000000, 1.000000000000000000 ) ) ;
#11585=DIRECTION ( 'NONE',  ( 1.000000000000000000, 0.000000000000000000, 0.000000000000000000 ) ) ;
#11618=FACE_OUTER_BOUND ( 'NONE', #12878, .T. ) ;
#11636=EDGE_CURVE ( 'NONE', #9335, #2497, #12735, .T. ) ;
#11705=DIRECTION ( 'NONE',  ( 0.000000000000000000, 0.4999999999999993339, -0.8660254037844390407 ) ) ;
#11717=TOROIDAL_SURFACE ( 'NONE', #14788, 4.000000000000000000, 0.2500000000000000000 ) ;
#11722=ORIENTED_EDGE ( 'NONE', *, *, #6255, .F. ) ;
#11732=PLANE ( 'NONE',  #5119 ) ;
#11759=ORIENTED_EDGE ( 'NONE', *, *, #8484, .T. ) ;
#11796=EDGE_CURVE ( 'NONE', #10466, #9335, #14611, .T. ) ;
#11820=DIRECTION ( 'NONE',  ( -1.000000000000000000, -0.000000000000000000, -0.000000000000000000 ) ) ;
#11852=PLANE ( 'NONE',  #5400 ) ;
#11882=ORIENTED_EDGE ( 'NONE', *, *, #5864, .T. ) ;
#11885=EDGE_CURVE ( 'NONE', #3698, #7837, #9440, .T. ) ;
#11897=CARTESIAN_POINT ( 'NONE',  ( 0.000000000000000000, 0.000000000000000000, 0.000000000000000000 ) ) ;
#11900=ORIENTED_EDGE ( 'NONE', *, *, #11025, .F. ) ;
#11911=CARTESIAN_POINT ( 'NONE',  ( 2.500000000000000000, -1.178949249685213863, 2.042000000000002924 ) ) ;
#11917=ORIENTED_EDGE ( 'NONE', *, *, #14232, .T. ) ;
#11971=FACE_OUTER_BOUND ( 'NONE', #7718, .T. ) ;
#11972=DIRECTION ( 'NONE',  ( 0.000000000000000000, 0.000000000000000000, 1.000000000000000000 ) ) ;
#11976=VECTOR ( 'NONE', #10082, 1000.000000000000000 ) ;
#11984=VECTOR ( 'NONE', #834, 1000.000000000000000 ) ;
#11997=SURFACE_SIDE_STYLE ('',( #12156 ) ) ;
#12022=VECTOR ( 'NONE', #221, 1000.000000000000000 ) ;
#12025=CIRCLE ( 'NONE', #2469, 2.700000000000000622 ) ;
#12043=ORIENTED_EDGE ( 'NONE', *, *, #14547, .T. ) ;
#12099=FACE_OUTER_BOUND ( 'NONE', #9228, .T. ) ;
#12113=FACE_OUTER_BOUND ( 'NONE', #14658, .T. ) ;
#12120=ORIENTED_EDGE ( 'NONE', *, *, #9564, .T. ) ;
#12123=FACE_OUTER_BOUND ( 'NONE', #6679, .T. ) ;
#12133=DIRECTION ( 'NONE',  ( 0.000000000000000000, 0.4999999999999993894, -0.8660254037844389297 ) ) ;
#12156=SURFACE_STYLE_FILL_AREA ( #9437 ) ;
#12160=EDGE_CURVE ( 'NONE', #1955, #13141, #10754, .T. ) ;
#12172=EDGE_LOOP ( 'NONE', ( #109, #11882 ) ) ;
#12177=ORIENTED_EDGE ( 'NONE', *, *, #13846, .F. ) ;
#12205=CARTESIAN_POINT ( 'NONE',  ( 0.000000000000000000, -2.357898499370432610, 3.252606517456513302E-15 ) ) ;
#12217=CARTESIAN_POINT ( 'NONE',  ( 2.500000000000000000, -2.629050547790028551E-15, -2.041999999999999815 ) ) ;
#12220=CARTESIAN_POINT ( 'NONE',  ( 0.000000000000000000, -1.178949249685218303, -2.041999999999998039 ) ) ;
#12271=ADVANCED_FACE ( 'NONE', ( #3997 ), #13772, .F. ) ;
#12291=LINE ( 'NONE', #2358, #9751 ) ;
#12299=CARTESIAN_POINT ( 'NONE',  ( 5.000000000000000888, 0.000000000000000000, 0.000000000000000000 ) ) ;
#12362=VECTOR ( 'NONE', #1216, 999.9999999999998863 ) ;
#12429=FACE_OUTER_BOUND ( 'NONE', #15116, .T. ) ;
#12438=EDGE_CURVE ( 'NONE', #3972, #1651, #12025, .T. ) ;
#12453=CIRCLE ( 'NONE', #6020, 2.500000000000000444 ) ;
#12457=VERTEX_POINT ( 'NONE', #8591 ) ;
#12505=PLANE ( 'NONE',  #2623 ) ;
#12513=VERTEX_POINT ( 'NONE', #4869 ) ;
#12530=VECTOR ( 'NONE', #15025, 1000.000000000000000 ) ;
#12545=LINE ( 'NONE', #1567, #13086 ) ;
#12553=DIRECTION ( 'NONE',  ( 0.000000000000000000, 0.000000000000000000, 1.000000000000000000 ) ) ;
#12556=EDGE_LOOP ( 'NONE', ( #5217, #6966, #11239, #6776, #7913 ) ) ;
#12581=CARTESIAN_POINT ( 'NONE',  ( 17.00000000000000000, 0.000000000000000000, 2.055000000000000160 ) ) ;
#12594=CARTESIAN_POINT ( 'NONE',  ( 0.2500000000000002220, 0.000000000000000000, 0.000000000000000000 ) ) ;
#12596=ORIENTED_EDGE ( 'NONE', *, *, #10086, .F. ) ;
#12637=VERTEX_POINT ( 'NONE', #7372 ) ;
#12642=EDGE_LOOP ( 'NONE', ( #8787, #8298, #12661 ) ) ;
#12644=DIRECTION ( 'NONE',  ( -0.000000000000000000, 1.471414886128461471E-15, 1.000000000000000000 ) ) ;
#12654=ORIENTED_EDGE ( 'NONE', *, *, #14245, .T. ) ;
#12655=CARTESIAN_POINT ( 'NONE',  ( 2.500000000000000000, 0.000000000000000000, 0.000000000000000000 ) ) ;
#12661=ORIENTED_EDGE ( 'NONE', *, *, #6147, .F. ) ;
#12663=LINE ( 'NONE', #332, #10310 ) ;
#12695=VECTOR ( 'NONE', #2837, 1000.000000000000000 ) ;
#12705=CARTESIAN_POINT ( 'NONE',  ( 17.00000000000000000, 0.000000000000000000, 2.055000000000000160 ) ) ;
#12710=AXIS2_PLACEMENT_3D ( 'NONE', #13191, #697, #5623 ) ;
#12712=ORIENTED_EDGE ( 'NONE', *, *, #8122, .F. ) ;
#12719=CARTESIAN_POINT ( 'NONE',  ( 2.500000000000000000, 1.178949249685213863, -2.042000000000001148 ) ) ;
#12735=LINE ( 'NONE', #12581, #12530 ) ;
#12770=LINE ( 'NONE', #1799, #2552 ) ;
#12775=EDGE_CURVE ( 'NONE', #15821, #2497, #194, .T. ) ;
#12782=FACE_OUTER_BOUND ( 'NONE', #6138, .T. ) ;
#12788=EDGE_LOOP ( 'NONE', ( #7659, #5559, #1795, #1310 ) ) ;
#12829=AXIS2_PLACEMENT_3D ( 'NONE', #1364, #9065, #412 ) ;
#12832=DIRECTION ( 'NONE',  ( 0.000000000000000000, -1.000000000000000000, 0.000000000000000000 ) ) ;
#12872=CARTESIAN_POINT ( 'NONE',  ( 2.500000000000000000, 2.357898499370433054, -1.951563910473907981E-15 ) ) ;
#12878=EDGE_LOOP ( 'NONE', ( #14566, #11722, #9926, #6875, #2938 ) ) ;
#12919=CARTESIAN_POINT ( 'NONE',  ( 0.000000000000000000, -2.357898499370432610, 3.252606517456513302E-15 ) ) ;
#12975=( NAMED_UNIT ( * ) SI_UNIT ( $, .STERADIAN. ) SOLID_ANGLE_UNIT ( ) );
#12995=DIRECTION ( 'NONE',  ( 0.000000000000000000, -0.5000000000000011102, -0.8660254037844379305 ) ) ;
#13028=AXIS2_PLACEMENT_3D ( 'NONE', #10060, #14989, #6262 ) ;
#13051=AXIS2_PLACEMENT_3D ( 'NONE', #12655, #13876, #14125 ) ;
#13057=SHAPE_REPRESENTATION_RELATIONSHIP ( 'NONE' , 'NONE' ,  #10906, #5806 ) ;
#13080=EDGE_LOOP ( 'NONE', ( #15750, #8455, #14321, #9901, #2207 ) ) ;
#13086=VECTOR ( 'NONE', #1492, 1000.000000000000114 ) ;
#13106=PRODUCT ( 'socket head cap screw_iso_ISO 4762 M5 x 12 - 12N', 'socket head cap screw_iso_ISO 4762 M5 x 12 - 12N', '', ( #7714 ) ) ;
#13141=VERTEX_POINT ( 'NONE', #11537 ) ;
#13171=DIRECTION ( 'NONE',  ( 0.000000000000000000, -0.5000000000000011102, -0.8660254037844379305 ) ) ;
#13191=CARTESIAN_POINT ( 'NONE',  ( 2.500000000000000000, 1.178949249685213863, -2.042000000000001148 ) ) ;
#13226=DIRECTION ( 'NONE',  ( 0.000000000000000000, 0.000000000000000000, -1.000000000000000000 ) ) ;
#13227=ORIENTED_EDGE ( 'NONE', *, *, #13750, .T. ) ;
#13262=CARTESIAN_POINT ( 'NONE',  ( 17.00000000000000000, 2.789133085058097101E-16, -2.055000000000000160 ) ) ;
#13263=VERTEX_POINT ( 'NONE', #4585 ) ;
#13284=TOROIDAL_SURFACE ( 'NONE', #6342, 2.700000000000000622, 0.2000000000000000111 ) ;
#13299=CARTESIAN_POINT ( 'NONE',  ( 5.000000000000002665, 0.000000000000000000, -2.700000000000000622 ) ) ;
#13326=EDGE_CURVE ( 'NONE', #7997, #1698, #10656, .T. ) ;
#13352=ORIENTED_EDGE ( 'NONE', *, *, #7586, .T. ) ;
#13394=ORIENTED_EDGE ( 'NONE', *, *, #10013, .F. ) ;
#13453=ORIENTED_EDGE ( 'NONE', *, *, #14547, .F. ) ;
#13459=EDGE_CURVE ( 'NONE', #6007, #3972, #14061, .T. ) ;
#13469=DIRECTION ( 'NONE',  ( -0.000000000000000000, 0.000000000000000000, 1.000000000000000000 ) ) ;
#13497=EDGE_CURVE ( 'NONE', #6259, #6791, #1584, .T. ) ;
#13502=DIRECTION ( 'NONE',  ( -1.000000000000000000, -0.000000000000000000, -0.000000000000000000 ) ) ;
#13526=AXIS2_PLACEMENT_3D ( 'NONE', #15861, #2113, #8359 ) ;
#13531=FACE_OUTER_BOUND ( 'NONE', #12788, .T. ) ;
#13544=DIRECTION ( 'NONE',  ( -1.000000000000000000, -0.000000000000000000, -0.000000000000000000 ) ) ;
#13565=AXIS2_PLACEMENT_3D ( 'NONE', #232, #13939, #15167 ) ;
#13575=AXIS2_PLACEMENT_3D ( 'NONE', #15123, #2836, #7788 ) ;
#13585=CIRCLE ( 'NONE', #15684, 2.041999999999999815 ) ;
#13643=DIRECTION ( 'NONE',  ( -1.000000000000000000, -0.000000000000000000, -0.000000000000000000 ) ) ;
#13686=DIRECTION ( 'NONE',  ( -1.000000000000000000, -0.000000000000000000, -0.000000000000000000 ) ) ;
#13698=DIRECTION ( 'NONE',  ( -1.000000000000000000, -0.000000000000000000, -0.000000000000000000 ) ) ;
#13699=PLANE ( 'NONE',  #8086 ) ;
#13700=DIRECTION ( 'NONE',  ( -1.000000000000000000, -0.000000000000000000, -0.000000000000000000 ) ) ;
#13713=DIRECTION ( 'NONE',  ( -1.000000000000000000, -0.000000000000000000, -0.000000000000000000 ) ) ;
#13750=EDGE_CURVE ( 'NONE', #6730, #11426, #2952, .T. ) ;
#13772=PLANE ( 'NONE',  #3006 ) ;
#13846=EDGE_CURVE ( 'NONE', #1651, #3972, #2182, .T. ) ;
#13870=DIRECTION ( 'NONE',  ( -1.000000000000000000, -0.000000000000000000, -0.000000000000000000 ) ) ;
#13876=DIRECTION ( 'NONE',  ( -1.000000000000000000, -0.000000000000000000, -0.000000000000000000 ) ) ;
#13877=EDGE_LOOP ( 'NONE', ( #9489, #6118, #3421, #12120, #9947 ) ) ;
#13894=CARTESIAN_POINT ( 'NONE',  ( 2.500000000000000000, 2.357898499370433054, -1.951563910473907981E-15 ) ) ;
#13902=ORIENTED_EDGE ( 'NONE', *, *, #10732, .T. ) ;
#13939=DIRECTION ( 'NONE',  ( -1.000000000000000000, -0.000000000000000000, -0.000000000000000000 ) ) ;
#14001=PRODUCT_DEFINITION_CONTEXT ( 'detailed design', #14352, 'design' ) ;
#14010=CARTESIAN_POINT ( 'NONE',  ( 2.500000000000000000, -2.357898499370432610, 3.252606517456513302E-15 ) ) ;
#14029=ADVANCED_FACE ( 'NONE', ( #4957 ), #6503, .F. ) ;
#14059=ORIENTED_EDGE ( 'NONE', *, *, #888, .F. ) ;
#14060=EDGE_LOOP ( 'NONE', ( #9657, #13902, #13453, #15959 ) ) ;
#14061=CIRCLE ( 'NONE', #6326, 0.2000000000000000944 ) ;
#14087=SURFACE_STYLE_USAGE ( .BOTH. , #9402 ) ;
#14097=MANIFOLD_SOLID_BREP ( 'Hex', #189 ) ;
#14125=DIRECTION ( 'NONE',  ( 0.000000000000000000, 0.000000000000000000, 1.000000000000000000 ) ) ;
#14142=AXIS2_PLACEMENT_3D ( 'NONE', #14476, #8346, #2180 ) ;
#14150=ORIENTED_EDGE ( 'NONE', *, *, #4049, .F. ) ;
#14172=VECTOR ( 'NONE', #11705, 1000.000000000000000 ) ;
#14216=DIRECTION ( 'NONE',  ( 0.000000000000000000, -1.000000000000000000, 1.287488025362403787E-15 ) ) ;
#14232=EDGE_CURVE ( 'NONE', #6791, #6707, #7061, .T. ) ;
#14245=EDGE_CURVE ( 'NONE', #4880, #1651, #2436, .T. ) ;
#14252=FILL_AREA_STYLE_COLOUR ( '', #6338 ) ;
#14261=EDGE_CURVE ( 'NONE', #9335, #10466, #7639, .T. ) ;
#14321=ORIENTED_EDGE ( 'NONE', *, *, #7586, .F. ) ;
#14352=APPLICATION_CONTEXT ( 'automotive_design' ) ;
#14364=ORIENTED_EDGE ( 'NONE', *, *, #819, .F. ) ;
#14374=PRODUCT_DEFINITION_FORMATION_WITH_SPECIFIED_SOURCE ( 'ANY', '', #13106, .NOT_KNOWN. ) ;
#14385=DIRECTION ( 'NONE',  ( 1.000000000000000000, 0.000000000000000000, 0.000000000000000000 ) ) ;
#14433=VECTOR ( 'NONE', #12995, 1000.000000000000114 ) ;
#14434=DIRECTION ( 'NONE',  ( 0.000000000000000000, 0.000000000000000000, -1.000000000000000000 ) ) ;
#14476=CARTESIAN_POINT ( 'NONE',  ( 5.000000000000004441, 0.000000000000000000, 0.000000000000000000 ) ) ;
#14501=VECTOR ( 'NONE', #10909, 1000.000000000000114 ) ;
#14510=DIRECTION ( 'NONE',  ( 0.000000000000000000, 0.000000000000000000, 1.000000000000000000 ) ) ;
#14523=AXIS2_PLACEMENT_3D ( 'NONE', #12594, #2901, #7852 ) ;
#14538=EDGE_LOOP ( 'NONE', ( #11917, #14059, #15005 ) ) ;
#14547=EDGE_CURVE ( 'NONE', #2497, #15821, #3478, .T. ) ;
#14559=CARTESIAN_POINT ( 'NONE',  ( 2.500000000000000000, 1.178949249685213863, -2.042000000000001148 ) ) ;
#14566=ORIENTED_EDGE ( 'NONE', *, *, #11025, .T. ) ;
#14589=VERTEX_POINT ( 'NONE', #15558 ) ;
#14594=AXIS2_PLACEMENT_3D ( 'NONE', #4596, #4755, #13226 ) ;
#14611=CIRCLE ( 'NONE', #8437, 2.055000000000000160 ) ;
#14627=VECTOR ( 'NONE', #14738, 1000.000000000000114 ) ;
#14658=EDGE_LOOP ( 'NONE', ( #12043, #6592, #15319, #14150 ) ) ;
#14660=CIRCLE ( 'NONE', #4600, 2.041999999999999815 ) ;
#14665=VECTOR ( 'NONE', #7469, 1000.000000000000114 ) ;
#14694=CARTESIAN_POINT ( 'NONE',  ( 2.500000000000000000, 2.357898499370433054, -1.951563910473907981E-15 ) ) ;
#14699=EDGE_LOOP ( 'NONE', ( #15965, #12712 ) ) ;
#14734=CARTESIAN_POINT ( 'NONE',  ( 2.500000000000000000, -1.178949249685213863, 2.042000000000002924 ) ) ;
#14738=DIRECTION ( 'NONE',  ( 0.000000000000000000, -0.4999999999999993894, 0.8660254037844389297 ) ) ;
#14762=EDGE_CURVE ( 'NONE', #6707, #7837, #7366, .T. ) ;
#14785=LINE ( 'NONE', #4765, #5632 ) ;
#14788=AXIS2_PLACEMENT_3D ( 'NONE', #5968, #15830, #1033 ) ;
#14793=VECTOR ( 'NONE', #8744, 1000.000000000000000 ) ;
#14795=CARTESIAN_POINT ( 'NONE',  ( 2.500000000000000000, -1.178949249685218303, -2.041999999999998039 ) ) ;
#14797=EDGE_LOOP ( 'NONE', ( #6658, #15771, #433, #5602 ) ) ;
#14889=TOROIDAL_SURFACE ( 'NONE', #2230, 4.000000000000000000, 0.2500000000000000000 ) ;
#14937=FACE_OUTER_BOUND ( 'NONE', #8600, .T. ) ;
#14989=DIRECTION ( 'NONE',  ( 1.000000000000000000, 0.000000000000000000, 0.000000000000000000 ) ) ;
#15005=ORIENTED_EDGE ( 'NONE', *, *, #4488, .F. ) ;
#15010=ADVANCED_FACE ( 'NONE', ( #12099 ), #13284, .F. ) ;
#15025=DIRECTION ( 'NONE',  ( -0.7071067811865369146, 0.000000000000000000, 0.7071067811865582309 ) ) ;
#15032=ADVANCED_FACE ( 'NONE', ( #2014 ), #889, .T. ) ;
#15038=FACE_OUTER_BOUND ( 'NONE', #14538, .T. ) ;
#15074=CARTESIAN_POINT ( 'NONE',  ( 16.55500000000001393, 3.061616997868383634E-16, -2.500000000000000444 ) ) ;
#15078=EDGE_CURVE ( 'NONE', #7896, #6730, #9946, .T. ) ;
#15086=DIRECTION ( 'NONE',  ( 1.000000000000000000, 0.000000000000000000, 0.000000000000000000 ) ) ;
#15101=AXIS2_PLACEMENT_3D ( 'NONE', #12299, #13502, #14434 ) ;
#15116=EDGE_LOOP ( 'NONE', ( #3621, #8420, #3338, #5116, #13227 ) ) ;
#15123=CARTESIAN_POINT ( 'NONE',  ( 16.55500000000001393, 0.000000000000000000, 0.000000000000000000 ) ) ;
#15124=AXIS2_PLACEMENT_3D ( 'NONE', #8270, #10435, #9540 ) ;
#15167=DIRECTION ( 'NONE',  ( 0.000000000000000000, 0.000000000000000000, 1.000000000000000000 ) ) ;
#15226=ORIENTED_EDGE ( 'NONE', *, *, #7377, .T. ) ;
#15242=DIRECTION ( 'NONE',  ( 0.000000000000000000, 0.000000000000000000, -1.000000000000000000 ) ) ;
#15280=DIRECTION ( 'NONE',  ( -1.000000000000000000, -0.000000000000000000, -0.000000000000000000 ) ) ;
#15282=DIRECTION ( 'NONE',  ( 0.000000000000000000, 0.000000000000000000, -1.000000000000000000 ) ) ;
#15319=ORIENTED_EDGE ( 'NONE', *, *, #3088, .T. ) ;
#15391=ADVANCED_FACE ( 'NONE', ( #2884 ), #8167, .F. ) ;
#15407=ORIENTED_EDGE ( 'NONE', *, *, #13846, .T. ) ;
#15420=FACE_OUTER_BOUND ( 'NONE', #3353, .T. ) ;
#15424=CONICAL_SURFACE ( 'NONE', #9004, 2.055000000000000160, 0.7853981633974633780 ) ;
#15446=CIRCLE ( 'NONE', #14142, 4.250000000000000000 ) ;
#15470=CIRCLE ( 'NONE', #10568, 2.041999999999999815 ) ;
#15503=DIRECTION ( 'NONE',  ( -1.000000000000000000, -0.000000000000000000, -0.000000000000000000 ) ) ;
#15558=CARTESIAN_POINT ( 'NONE',  ( 2.500000000000000000, 2.357898499370433054, -1.951563910473907981E-15 ) ) ;
#15573=DIRECTION ( 'NONE',  ( 0.000000000000000000, 0.000000000000000000, -1.000000000000000000 ) ) ;
#15636=CARTESIAN_POINT ( 'NONE',  ( 2.500000000000000000, -2.357898499370432610, 3.252606517456513302E-15 ) ) ;
#15684=AXIS2_PLACEMENT_3D ( 'NONE', #3179, #3108, #4397 ) ;
#15704=VECTOR ( 'NONE', #15503, 1000.000000000000000 ) ;
#15725=CARTESIAN_POINT ( 'NONE',  ( 2.500000000000000000, 2.357898499370433054, -1.951563910473907981E-15 ) ) ;
#15750=ORIENTED_EDGE ( 'NONE', *, *, #9855, .T. ) ;
#15771=ORIENTED_EDGE ( 'NONE', *, *, #12775, .T. ) ;
#15821=VERTEX_POINT ( 'NONE', #15074 ) ;
#15830=DIRECTION ( 'NONE',  ( -1.000000000000000000, -0.000000000000000000, -0.000000000000000000 ) ) ;
#15860=ORIENTED_EDGE ( 'NONE', *, *, #10086, .T. ) ;
#15861=CARTESIAN_POINT ( 'NONE',  ( 17.00000000000000000, 0.000000000000000000, 0.000000000000000000 ) ) ;
#15888=CARTESIAN_POINT ( 'NONE',  ( 2.500000000000000000, -1.768423874527823791, -1.020999999999998353 ) ) ;
#15911=LINE ( 'NONE', #14694, #9879 ) ;
#15942=DIRECTION ( 'NONE',  ( 1.000000000000000000, 0.000000000000000000, 0.000000000000000000 ) ) ;
#15949=CIRCLE ( 'NONE', #4064, 2.500000000000000444 ) ;
#15959=ORIENTED_EDGE ( 'NONE', *, *, #11636, .F. ) ;
#15965=ORIENTED_EDGE ( 'NONE', *, *, #3086, .F. ) ;
ENDSEC;
END-ISO-10303-21;
